ISO-10303-21;
HEADER;
/* Generated by software containing ST-Developer
 * from STEP Tools, Inc. (www.steptools.com) 
 */

FILE_DESCRIPTION(
/* description */ ('Bin tilter linkage'),
/* implementation_level */ '2;1');

FILE_NAME(
/* name */ 'M4 short cap screw (29).step',
/* time_stamp */ '2026-10-28T03:26:24-07:00',
/* author */ (''),
/* organization */ (''),
/* preprocessor_version */ 'ST-DEVELOPER v20.2',
/* originating_system */ 'Autodesk Translation Framework v15.17.0.0',
/* authorisation */ '');

FILE_SCHEMA (('AUTOMOTIVE_DESIGN { 1 0 10303 214 3 1 1 }'));
ENDSEC;

DATA;
#10=MECHANICAL_DESIGN_GEOMETRIC_PRESENTATION_REPRESENTATION('',(#931),#23728);
#719=SHAPE_REPRESENTATION_RELATIONSHIP('SRR','None',#24185,#825);
#825=ADVANCED_BREP_SHAPE_REPRESENTATION('',(#1044),#23685);
#931=STYLED_ITEM('',(#24772),#1044);
#1044=MANIFOLD_SOLID_BREP('Body1',#12462);
#1383=FACE_BOUND('',#3454,.T.);
#1728=PLANE('',#14744);
#1729=PLANE('',#14749);
#1730=PLANE('',#14752);
#2380=FACE_OUTER_BOUND('',#3453,.T.);
#2381=FACE_OUTER_BOUND('',#3455,.T.);
#2382=FACE_OUTER_BOUND('',#3456,.T.);
#2383=FACE_OUTER_BOUND('',#3457,.T.);
#2384=FACE_OUTER_BOUND('',#3458,.T.);
#3453=EDGE_LOOP('',(#10177));
#3454=EDGE_LOOP('',(#10178));
#3455=EDGE_LOOP('',(#10179,#10180,#10181,#10182));
#3456=EDGE_LOOP('',(#10183));
#3457=EDGE_LOOP('',(#10184,#10185,#10186,#10187));
#3458=EDGE_LOOP('',(#10188));
#4247=LINE('',#21819,#4922);
#4248=LINE('',#21823,#4923);
#4922=VECTOR('',#18018,0.350000000000001);
#4923=VECTOR('',#18023,0.199999999999999);
#5703=CIRCLE('',#14745,0.350000000000001);
#5704=CIRCLE('',#14746,0.199999999999999);
#5705=CIRCLE('',#14748,0.350000000000001);
#5706=CIRCLE('',#14751,0.199999999999999);
#6557=VERTEX_POINT('',#21812);
#6558=VERTEX_POINT('',#21814);
#6559=VERTEX_POINT('',#21817);
#6560=VERTEX_POINT('',#21822);
#7828=EDGE_CURVE('',#6557,#6557,#5703,.T.);
#7829=EDGE_CURVE('',#6558,#6558,#5704,.T.);
#7830=EDGE_CURVE('',#6559,#6559,#5705,.T.);
#7831=EDGE_CURVE('',#6559,#6557,#4247,.T.);
#7832=EDGE_CURVE('',#6558,#6560,#4248,.T.);
#7833=EDGE_CURVE('',#6560,#6560,#5706,.T.);
#10177=ORIENTED_EDGE('',*,*,#7828,.F.);
#10178=ORIENTED_EDGE('',*,*,#7829,.T.);
#10179=ORIENTED_EDGE('',*,*,#7830,.F.);
#10180=ORIENTED_EDGE('',*,*,#7831,.T.);
#10181=ORIENTED_EDGE('',*,*,#7828,.T.);
#10182=ORIENTED_EDGE('',*,*,#7831,.F.);
#10183=ORIENTED_EDGE('',*,*,#7830,.T.);
#10184=ORIENTED_EDGE('',*,*,#7829,.F.);
#10185=ORIENTED_EDGE('',*,*,#7832,.T.);
#10186=ORIENTED_EDGE('',*,*,#7833,.T.);
#10187=ORIENTED_EDGE('',*,*,#7832,.F.);
#10188=ORIENTED_EDGE('',*,*,#7833,.F.);
#11517=CYLINDRICAL_SURFACE('',#14747,0.350000000000001);
#11518=CYLINDRICAL_SURFACE('',#14750,0.199999999999999);
#12105=ADVANCED_FACE('',(#2380,#1383),#1728,.F.);
#12106=ADVANCED_FACE('',(#2381),#11517,.T.);
#12107=ADVANCED_FACE('',(#2382),#1729,.T.);
#12108=ADVANCED_FACE('',(#2383),#11518,.T.);
#12109=ADVANCED_FACE('',(#2384),#1730,.F.);
#12462=CLOSED_SHELL('',(#12105,#12106,#12107,#12108,#12109));
#14743=AXIS2_PLACEMENT_3D('',#21810,#18006,#18007);
#14744=AXIS2_PLACEMENT_3D('',#21811,#18008,#18009);
#14745=AXIS2_PLACEMENT_3D('',#21813,#18010,#18011);
#14746=AXIS2_PLACEMENT_3D('',#21815,#18012,#18013);
#14747=AXIS2_PLACEMENT_3D('',#21816,#18014,#18015);
#14748=AXIS2_PLACEMENT_3D('',#21818,#18016,#18017);
#14749=AXIS2_PLACEMENT_3D('',#21820,#18019,#18020);
#14750=AXIS2_PLACEMENT_3D('',#21821,#18021,#18022);
#14751=AXIS2_PLACEMENT_3D('',#21824,#18024,#18025);
#14752=AXIS2_PLACEMENT_3D('',#21825,#18026,#18027);
#18006=DIRECTION('axis',(0.,0.,1.));
#18007=DIRECTION('refdir',(1.,0.,0.));
#18008=DIRECTION('center_axis',(0.,1.,0.));
#18009=DIRECTION('ref_axis',(1.,0.,0.));
#18010=DIRECTION('center_axis',(0.,1.,0.));
#18011=DIRECTION('ref_axis',(1.,0.,0.));
#18012=DIRECTION('center_axis',(0.,1.,0.));
#18013=DIRECTION('ref_axis',(1.,0.,0.));
#18014=DIRECTION('center_axis',(0.,1.,0.));
#18015=DIRECTION('ref_axis',(1.,0.,0.));
#18016=DIRECTION('center_axis',(0.,1.,0.));
#18017=DIRECTION('ref_axis',(1.,0.,0.));
#18018=DIRECTION('',(0.,-1.,0.));
#18019=DIRECTION('center_axis',(0.,1.,0.));
#18020=DIRECTION('ref_axis',(1.,0.,0.));
#18021=DIRECTION('center_axis',(0.,1.,0.));
#18022=DIRECTION('ref_axis',(1.,0.,0.));
#18023=DIRECTION('',(0.,-1.,0.));
#18024=DIRECTION('center_axis',(0.,1.,0.));
#18025=DIRECTION('ref_axis',(1.,0.,0.));
#18026=DIRECTION('center_axis',(0.,1.,0.));
#18027=DIRECTION('ref_axis',(1.,0.,0.));
#21810=CARTESIAN_POINT('',(0.,0.,0.));
#21811=CARTESIAN_POINT('Origin',(22.893930933827,0.8,29.9659007476824));
#21812=CARTESIAN_POINT('',(22.543930933827,0.8,29.9659007476824));
#21813=CARTESIAN_POINT('Origin',(22.893930933827,0.8,29.9659007476824));
#21814=CARTESIAN_POINT('',(22.693930933827,0.8,29.9659007476824));
#21815=CARTESIAN_POINT('Origin',(22.893930933827,0.8,29.9659007476824));
#21816=CARTESIAN_POINT('Origin',(22.893930933827,0.8,29.9659007476824));
#21817=CARTESIAN_POINT('',(22.543930933827,1.2,29.9659007476824));
#21818=CARTESIAN_POINT('Origin',(22.893930933827,1.2,29.9659007476824));
#21819=CARTESIAN_POINT('',(22.543930933827,0.8,29.9659007476824));
#21820=CARTESIAN_POINT('Origin',(22.893930933827,1.2,29.9659007476824));
#21821=CARTESIAN_POINT('Origin',(22.893930933827,0.1,29.9659007476824));
#21822=CARTESIAN_POINT('',(22.693930933827,0.1,29.9659007476824));
#21823=CARTESIAN_POINT('',(22.693930933827,0.1,29.9659007476824));
#21824=CARTESIAN_POINT('Origin',(22.893930933827,0.1,29.9659007476824));
#21825=CARTESIAN_POINT('Origin',(22.893930933827,0.1,29.9659007476824));
#23568=UNCERTAINTY_MEASURE_WITH_UNIT(LENGTH_MEASURE(0.001),#23729,
'DISTANCE_ACCURACY_VALUE',
'Maximum model space distance between geometric entities at asserted c
onnectivities');
#23611=UNCERTAINTY_MEASURE_WITH_UNIT(LENGTH_MEASURE(0.001),#23729,
'DISTANCE_ACCURACY_VALUE',
'Maximum model space distance between geometric entities at asserted c
onnectivities');
#23685=(
GEOMETRIC_REPRESENTATION_CONTEXT(3)
GLOBAL_UNCERTAINTY_ASSIGNED_CONTEXT((#23568))
GLOBAL_UNIT_ASSIGNED_CONTEXT((#23729,#23731,#23732))
REPRESENTATION_CONTEXT('','3D')
);
#23728=(
GEOMETRIC_REPRESENTATION_CONTEXT(3)
GLOBAL_UNCERTAINTY_ASSIGNED_CONTEXT((#23611))
GLOBAL_UNIT_ASSIGNED_CONTEXT((#23729,#23731,#23732))
REPRESENTATION_CONTEXT('','3D')
);
#23729=(
LENGTH_UNIT()
NAMED_UNIT(*)
SI_UNIT(.CENTI.,.METRE.)
);
#23731=(
NAMED_UNIT(*)
PLANE_ANGLE_UNIT()
SI_UNIT($,.RADIAN.)
);
#23732=(
NAMED_UNIT(*)
SI_UNIT($,.STERADIAN.)
SOLID_ANGLE_UNIT()
);
#23806=SHAPE_DEFINITION_REPRESENTATION(#23922,#24185);
#23922=PRODUCT_DEFINITION_SHAPE('',$,#24302);
#24185=SHAPE_REPRESENTATION('',(#14743),#23685);
#24228=PRODUCT_DEFINITION_CONTEXT('part definition',#24578,'design');
#24302=PRODUCT_DEFINITION('M4 short cap screw (29)',
'M4 short cap screw (29)',#24418,#24228);
#24418=PRODUCT_DEFINITION_FORMATION('',$,#24653);
#24578=APPLICATION_CONTEXT(
'Core Data for Automotive Mechanical Design Process');
#24579=PRODUCT_CONTEXT('part definition',#24578,'mechanical');
#24653=PRODUCT('M4 short cap screw (29)','M4 short cap screw (29)',
'M4 short cap screw (29)',(#24579));
#24766=COLOUR_RGB('Black',0.12,0.14,0.17);
#24767=FILL_AREA_STYLE_COLOUR('',#24766);
#24768=FILL_AREA_STYLE('',(#24767));
#24769=SURFACE_STYLE_FILL_AREA(#24768);
#24770=SURFACE_SIDE_STYLE('',(#24769));
#24771=SURFACE_STYLE_USAGE(.BOTH.,#24770);
#24772=PRESENTATION_STYLE_ASSIGNMENT((#24771));
ENDSEC;
END-ISO-10303-21;
